ISO-10303-21;
HEADER;
/* Generated by software containing ST-Developer
 * from STEP Tools, Inc. (www.steptools.com) 
 */

FILE_DESCRIPTION(
/* description */ ('PAT-091'),
/* implementation_level */ '2;1');

FILE_NAME(
/* name */ 'Axle distance sleeve 5 mm (3).step',
/* time_stamp */ '2026-10-27T15:34:44-07:00',
/* author */ (''),
/* organization */ (''),
/* preprocessor_version */ 'ST-DEVELOPER v20.2',
/* originating_system */ 'Autodesk Translation Framework v15.17.0.0',
/* authorisation */ '');

FILE_SCHEMA (('AUTOMOTIVE_DESIGN { 1 0 10303 214 3 1 1 }'));
ENDSEC;

DATA;
#10=MECHANICAL_DESIGN_GEOMETRIC_PRESENTATION_REPRESENTATION('',(#998),#25100);
#778=SHAPE_REPRESENTATION_RELATIONSHIP('SRR','None',#25540,#888);
#888=ADVANCED_BREP_SHAPE_REPRESENTATION('',(#1121),#25010);
#998=STYLED_ITEM('',(#26191),#1121);
#1121=MANIFOLD_SOLID_BREP('Body1',#13276);
#1385=FACE_BOUND('',#3285,.T.);
#1386=FACE_BOUND('',#3287,.T.);
#1760=PLANE('',#15072);
#1761=PLANE('',#15073);
#2294=FACE_OUTER_BOUND('',#3282,.T.);
#2295=FACE_OUTER_BOUND('',#3283,.T.);
#2296=FACE_OUTER_BOUND('',#3284,.T.);
#2297=FACE_OUTER_BOUND('',#3286,.T.);
#3282=EDGE_LOOP('',(#9956,#9957,#9958,#9959));
#3283=EDGE_LOOP('',(#9960,#9961,#9962,#9963));
#3284=EDGE_LOOP('',(#9964));
#3285=EDGE_LOOP('',(#9965));
#3286=EDGE_LOOP('',(#9966));
#3287=EDGE_LOOP('',(#9967));
#4397=LINE('',#22059,#5137);
#4398=LINE('',#22065,#5138);
#5137=VECTOR('',#17707,0.605);
#5138=VECTOR('',#17714,0.8);
#5823=CIRCLE('',#15067,0.605);
#5824=CIRCLE('',#15068,0.605);
#5825=CIRCLE('',#15070,0.8);
#5826=CIRCLE('',#15071,0.8);
#6710=VERTEX_POINT('',#22056);
#6711=VERTEX_POINT('',#22058);
#6712=VERTEX_POINT('',#22062);
#6713=VERTEX_POINT('',#22064);
#7913=EDGE_CURVE('',#6710,#6710,#5823,.T.);
#7914=EDGE_CURVE('',#6710,#6711,#4397,.T.);
#7915=EDGE_CURVE('',#6711,#6711,#5824,.T.);
#7916=EDGE_CURVE('',#6712,#6712,#5825,.T.);
#7917=EDGE_CURVE('',#6712,#6713,#4398,.T.);
#7918=EDGE_CURVE('',#6713,#6713,#5826,.T.);
#9956=ORIENTED_EDGE('',*,*,#7913,.F.);
#9957=ORIENTED_EDGE('',*,*,#7914,.T.);
#9958=ORIENTED_EDGE('',*,*,#7915,.T.);
#9959=ORIENTED_EDGE('',*,*,#7914,.F.);
#9960=ORIENTED_EDGE('',*,*,#7916,.F.);
#9961=ORIENTED_EDGE('',*,*,#7917,.T.);
#9962=ORIENTED_EDGE('',*,*,#7918,.T.);
#9963=ORIENTED_EDGE('',*,*,#7917,.F.);
#9964=ORIENTED_EDGE('',*,*,#7916,.T.);
#9965=ORIENTED_EDGE('',*,*,#7913,.T.);
#9966=ORIENTED_EDGE('',*,*,#7918,.F.);
#9967=ORIENTED_EDGE('',*,*,#7915,.F.);
#12182=CYLINDRICAL_SURFACE('',#15066,0.605);
#12183=CYLINDRICAL_SURFACE('',#15069,0.8);
#12661=ADVANCED_FACE('',(#2294),#12182,.F.);
#12662=ADVANCED_FACE('',(#2295),#12183,.T.);
#12663=ADVANCED_FACE('',(#2296,#1385),#1760,.T.);
#12664=ADVANCED_FACE('',(#2297,#1386),#1761,.F.);
#13276=CLOSED_SHELL('',(#12661,#12662,#12663,#12664));
#15065=AXIS2_PLACEMENT_3D('',#22054,#17701,#17702);
#15066=AXIS2_PLACEMENT_3D('',#22055,#17703,#17704);
#15067=AXIS2_PLACEMENT_3D('',#22057,#17705,#17706);
#15068=AXIS2_PLACEMENT_3D('',#22060,#17708,#17709);
#15069=AXIS2_PLACEMENT_3D('',#22061,#17710,#17711);
#15070=AXIS2_PLACEMENT_3D('',#22063,#17712,#17713);
#15071=AXIS2_PLACEMENT_3D('',#22066,#17715,#17716);
#15072=AXIS2_PLACEMENT_3D('',#22067,#17717,#17718);
#15073=AXIS2_PLACEMENT_3D('',#22068,#17719,#17720);
#17701=DIRECTION('axis',(0.,0.,1.));
#17702=DIRECTION('refdir',(1.,0.,0.));
#17703=DIRECTION('center_axis',(0.,1.,0.));
#17704=DIRECTION('ref_axis',(1.,0.,0.));
#17705=DIRECTION('center_axis',(0.,-1.,0.));
#17706=DIRECTION('ref_axis',(1.,0.,0.));
#17707=DIRECTION('',(0.,-1.,0.));
#17708=DIRECTION('center_axis',(0.,-1.,0.));
#17709=DIRECTION('ref_axis',(1.,0.,0.));
#17710=DIRECTION('center_axis',(0.,1.,0.));
#17711=DIRECTION('ref_axis',(1.,0.,0.));
#17712=DIRECTION('center_axis',(0.,1.,0.));
#17713=DIRECTION('ref_axis',(1.,0.,0.));
#17714=DIRECTION('',(0.,-1.,0.));
#17715=DIRECTION('center_axis',(0.,1.,0.));
#17716=DIRECTION('ref_axis',(1.,0.,0.));
#17717=DIRECTION('center_axis',(0.,1.,0.));
#17718=DIRECTION('ref_axis',(1.,0.,0.));
#17719=DIRECTION('center_axis',(0.,1.,0.));
#17720=DIRECTION('ref_axis',(1.,0.,0.));
#22054=CARTESIAN_POINT('',(0.,0.,0.));
#22055=CARTESIAN_POINT('Origin',(0.,-4.5,13.));
#22056=CARTESIAN_POINT('',(-0.605,-4.,13.));
#22057=CARTESIAN_POINT('Origin',(0.,-4.,13.));
#22058=CARTESIAN_POINT('',(-0.605,-4.5,13.));
#22059=CARTESIAN_POINT('',(-0.605,-4.5,13.));
#22060=CARTESIAN_POINT('Origin',(0.,-4.5,13.));
#22061=CARTESIAN_POINT('Origin',(0.,-4.5,13.));
#22062=CARTESIAN_POINT('',(-0.8,-4.,13.));
#22063=CARTESIAN_POINT('Origin',(0.,-4.,13.));
#22064=CARTESIAN_POINT('',(-0.8,-4.5,13.));
#22065=CARTESIAN_POINT('',(-0.8,-4.5,13.));
#22066=CARTESIAN_POINT('Origin',(0.,-4.5,13.));
#22067=CARTESIAN_POINT('Origin',(0.,-4.,13.));
#22068=CARTESIAN_POINT('Origin',(0.,-4.5,13.));
#24889=UNCERTAINTY_MEASURE_WITH_UNIT(LENGTH_MEASURE(0.001),#25101,
'DISTANCE_ACCURACY_VALUE',
'Maximum model space distance between geometric entities at asserted c
onnectivities');
#24979=UNCERTAINTY_MEASURE_WITH_UNIT(LENGTH_MEASURE(0.001),#25101,
'DISTANCE_ACCURACY_VALUE',
'Maximum model space distance between geometric entities at asserted c
onnectivities');
#25010=(
GEOMETRIC_REPRESENTATION_CONTEXT(3)
GLOBAL_UNCERTAINTY_ASSIGNED_CONTEXT((#24889))
GLOBAL_UNIT_ASSIGNED_CONTEXT((#25101,#25103,#25104))
REPRESENTATION_CONTEXT('','3D')
);
#25100=(
GEOMETRIC_REPRESENTATION_CONTEXT(3)
GLOBAL_UNCERTAINTY_ASSIGNED_CONTEXT((#24979))
GLOBAL_UNIT_ASSIGNED_CONTEXT((#25101,#25103,#25104))
REPRESENTATION_CONTEXT('','3D')
);
#25101=(
LENGTH_UNIT()
NAMED_UNIT(*)
SI_UNIT(.CENTI.,.METRE.)
);
#25103=(
NAMED_UNIT(*)
PLANE_ANGLE_UNIT()
SI_UNIT($,.RADIAN.)
);
#25104=(
NAMED_UNIT(*)
SI_UNIT($,.STERADIAN.)
SOLID_ANGLE_UNIT()
);
#25135=SHAPE_DEFINITION_REPRESENTATION(#25255,#25540);
#25255=PRODUCT_DEFINITION_SHAPE('',$,#25661);
#25540=SHAPE_REPRESENTATION('',(#15065),#25010);
#25630=PRODUCT_DEFINITION_CONTEXT('part definition',#25992,'design');
#25661=PRODUCT_DEFINITION('Axle distance sleeve 5 mm (3)',
'Axle distance sleeve 5 mm (3)',#25781,#25630);
#25781=PRODUCT_DEFINITION_FORMATION('',$,#26024);
#25992=APPLICATION_CONTEXT(
'Core Data for Automotive Mechanical Design Process');
#25993=PRODUCT_CONTEXT('part definition',#25992,'mechanical');
#26024=PRODUCT('Axle distance sleeve 5 mm (3)',
'Axle distance sleeve 5 mm (3)','Axle distance sleeve 5 mm (3)',(#25993));
#26185=COLOUR_RGB('Grey',0.48,0.52,0.57);
#26186=FILL_AREA_STYLE_COLOUR('',#26185);
#26187=FILL_AREA_STYLE('',(#26186));
#26188=SURFACE_STYLE_FILL_AREA(#26187);
#26189=SURFACE_SIDE_STYLE('',(#26188));
#26190=SURFACE_STYLE_USAGE(.BOTH.,#26189);
#26191=PRESENTATION_STYLE_ASSIGNMENT((#26190));
ENDSEC;
END-ISO-10303-21;
